ISO-10303-21;
HEADER;
/* Generated by software containing ST-Developer
 * from STEP Tools, Inc. (www.steptools.com) 
 */

FILE_DESCRIPTION(
/* description */ ('Bracket-mounted idler roller'),
/* implementation_level */ '2;1');

FILE_NAME(
/* name */ 'Journal spacer (1).step',
/* time_stamp */ '2026-10-28T03:26:42-07:00',
/* author */ (''),
/* organization */ (''),
/* preprocessor_version */ 'ST-DEVELOPER v20.2',
/* originating_system */ 'Autodesk Translation Framework v15.17.0.0',
/* authorisation */ '');

FILE_SCHEMA (('AUTOMOTIVE_DESIGN { 1 0 10303 214 3 1 1 }'));
ENDSEC;

DATA;
#10=MECHANICAL_DESIGN_GEOMETRIC_PRESENTATION_REPRESENTATION('',(#284),#6241);
#242=SHAPE_REPRESENTATION_RELATIONSHIP('SRR','None',#6346,#263);
#263=ADVANCED_BREP_SHAPE_REPRESENTATION('',(#313),#6222);
#284=STYLED_ITEM('',(#6531),#313);
#313=MANIFOLD_SOLID_BREP('Body1',#3186);
#356=FACE_BOUND('',#773,.T.);
#357=FACE_BOUND('',#775,.T.);
#447=PLANE('',#3527);
#448=PLANE('',#3528);
#559=FACE_OUTER_BOUND('',#770,.T.);
#560=FACE_OUTER_BOUND('',#771,.T.);
#561=FACE_OUTER_BOUND('',#772,.T.);
#562=FACE_OUTER_BOUND('',#774,.T.);
#770=EDGE_LOOP('',(#2340,#2341,#2342,#2343));
#771=EDGE_LOOP('',(#2344,#2345,#2346,#2347));
#772=EDGE_LOOP('',(#2348));
#773=EDGE_LOOP('',(#2349));
#774=EDGE_LOOP('',(#2350));
#775=EDGE_LOOP('',(#2351));
#1040=LINE('',#5149,#1222);
#1041=LINE('',#5155,#1223);
#1222=VECTOR('',#4103,0.505);
#1223=VECTOR('',#4110,0.8);
#1369=CIRCLE('',#3522,0.505);
#1370=CIRCLE('',#3523,0.505);
#1371=CIRCLE('',#3525,0.8);
#1372=CIRCLE('',#3526,0.8);
#1582=VERTEX_POINT('',#5146);
#1583=VERTEX_POINT('',#5148);
#1584=VERTEX_POINT('',#5152);
#1585=VERTEX_POINT('',#5154);
#1872=EDGE_CURVE('',#1582,#1582,#1369,.T.);
#1873=EDGE_CURVE('',#1582,#1583,#1040,.T.);
#1874=EDGE_CURVE('',#1583,#1583,#1370,.T.);
#1875=EDGE_CURVE('',#1584,#1584,#1371,.T.);
#1876=EDGE_CURVE('',#1584,#1585,#1041,.T.);
#1877=EDGE_CURVE('',#1585,#1585,#1372,.T.);
#2340=ORIENTED_EDGE('',*,*,#1872,.F.);
#2341=ORIENTED_EDGE('',*,*,#1873,.T.);
#2342=ORIENTED_EDGE('',*,*,#1874,.T.);
#2343=ORIENTED_EDGE('',*,*,#1873,.F.);
#2344=ORIENTED_EDGE('',*,*,#1875,.F.);
#2345=ORIENTED_EDGE('',*,*,#1876,.T.);
#2346=ORIENTED_EDGE('',*,*,#1877,.T.);
#2347=ORIENTED_EDGE('',*,*,#1876,.F.);
#2348=ORIENTED_EDGE('',*,*,#1875,.T.);
#2349=ORIENTED_EDGE('',*,*,#1872,.T.);
#2350=ORIENTED_EDGE('',*,*,#1877,.F.);
#2351=ORIENTED_EDGE('',*,*,#1874,.F.);
#2941=CYLINDRICAL_SURFACE('',#3521,0.505);
#2942=CYLINDRICAL_SURFACE('',#3524,0.8);
#3034=ADVANCED_FACE('',(#559),#2941,.F.);
#3035=ADVANCED_FACE('',(#560),#2942,.T.);
#3036=ADVANCED_FACE('',(#561,#356),#447,.T.);
#3037=ADVANCED_FACE('',(#562,#357),#448,.F.);
#3186=CLOSED_SHELL('',(#3034,#3035,#3036,#3037));
#3520=AXIS2_PLACEMENT_3D('',#5144,#4097,#4098);
#3521=AXIS2_PLACEMENT_3D('',#5145,#4099,#4100);
#3522=AXIS2_PLACEMENT_3D('',#5147,#4101,#4102);
#3523=AXIS2_PLACEMENT_3D('',#5150,#4104,#4105);
#3524=AXIS2_PLACEMENT_3D('',#5151,#4106,#4107);
#3525=AXIS2_PLACEMENT_3D('',#5153,#4108,#4109);
#3526=AXIS2_PLACEMENT_3D('',#5156,#4111,#4112);
#3527=AXIS2_PLACEMENT_3D('',#5157,#4113,#4114);
#3528=AXIS2_PLACEMENT_3D('',#5158,#4115,#4116);
#4097=DIRECTION('axis',(0.,0.,1.));
#4098=DIRECTION('refdir',(1.,0.,0.));
#4099=DIRECTION('center_axis',(0.,1.,0.));
#4100=DIRECTION('ref_axis',(1.,0.,0.));
#4101=DIRECTION('center_axis',(0.,-1.,0.));
#4102=DIRECTION('ref_axis',(1.,0.,0.));
#4103=DIRECTION('',(0.,-1.,0.));
#4104=DIRECTION('center_axis',(0.,-1.,0.));
#4105=DIRECTION('ref_axis',(1.,0.,0.));
#4106=DIRECTION('center_axis',(0.,1.,0.));
#4107=DIRECTION('ref_axis',(1.,0.,0.));
#4108=DIRECTION('center_axis',(0.,1.,0.));
#4109=DIRECTION('ref_axis',(1.,0.,0.));
#4110=DIRECTION('',(0.,-1.,0.));
#4111=DIRECTION('center_axis',(0.,1.,0.));
#4112=DIRECTION('ref_axis',(1.,0.,0.));
#4113=DIRECTION('center_axis',(0.,1.,0.));
#4114=DIRECTION('ref_axis',(1.,0.,0.));
#4115=DIRECTION('center_axis',(0.,1.,0.));
#4116=DIRECTION('ref_axis',(1.,0.,0.));
#5144=CARTESIAN_POINT('',(0.,0.,0.));
#5145=CARTESIAN_POINT('Origin',(0.,30.,4.5));
#5146=CARTESIAN_POINT('',(-0.505,31.6,4.5));
#5147=CARTESIAN_POINT('Origin',(0.,31.6,4.5));
#5148=CARTESIAN_POINT('',(-0.505,30.,4.5));
#5149=CARTESIAN_POINT('',(-0.505,30.,4.5));
#5150=CARTESIAN_POINT('Origin',(0.,30.,4.5));
#5151=CARTESIAN_POINT('Origin',(0.,30.,4.5));
#5152=CARTESIAN_POINT('',(-0.8,31.6,4.5));
#5153=CARTESIAN_POINT('Origin',(0.,31.6,4.5));
#5154=CARTESIAN_POINT('',(-0.8,30.,4.5));
#5155=CARTESIAN_POINT('',(-0.8,30.,4.5));
#5156=CARTESIAN_POINT('Origin',(0.,30.,4.5));
#5157=CARTESIAN_POINT('Origin',(0.,31.6,4.5));
#5158=CARTESIAN_POINT('Origin',(0.,30.,4.5));
#6196=UNCERTAINTY_MEASURE_WITH_UNIT(LENGTH_MEASURE(0.001),#6242,
'DISTANCE_ACCURACY_VALUE',
'Maximum model space distance between geometric entities at asserted c
onnectivities');
#6215=UNCERTAINTY_MEASURE_WITH_UNIT(LENGTH_MEASURE(0.001),#6242,
'DISTANCE_ACCURACY_VALUE',
'Maximum model space distance between geometric entities at asserted c
onnectivities');
#6222=(
GEOMETRIC_REPRESENTATION_CONTEXT(3)
GLOBAL_UNCERTAINTY_ASSIGNED_CONTEXT((#6196))
GLOBAL_UNIT_ASSIGNED_CONTEXT((#6242,#6244,#6245))
REPRESENTATION_CONTEXT('','3D')
);
#6241=(
GEOMETRIC_REPRESENTATION_CONTEXT(3)
GLOBAL_UNCERTAINTY_ASSIGNED_CONTEXT((#6215))
GLOBAL_UNIT_ASSIGNED_CONTEXT((#6242,#6244,#6245))
REPRESENTATION_CONTEXT('','3D')
);
#6242=(
LENGTH_UNIT()
NAMED_UNIT(*)
SI_UNIT(.CENTI.,.METRE.)
);
#6244=(
NAMED_UNIT(*)
PLANE_ANGLE_UNIT()
SI_UNIT($,.RADIAN.)
);
#6245=(
NAMED_UNIT(*)
SI_UNIT($,.STERADIAN.)
SOLID_ANGLE_UNIT()
);
#6252=SHAPE_DEFINITION_REPRESENTATION(#6277,#6346);
#6277=PRODUCT_DEFINITION_SHAPE('',$,#6372);
#6346=SHAPE_REPRESENTATION('',(#3520),#6222);
#6365=PRODUCT_DEFINITION_CONTEXT('part definition',#6442,'design');
#6372=PRODUCT_DEFINITION('Journal spacer (1)','Journal spacer (1)',#6397,
#6365);
#6397=PRODUCT_DEFINITION_FORMATION('',$,#6450);
#6442=APPLICATION_CONTEXT(
'Core Data for Automotive Mechanical Design Process');
#6443=PRODUCT_CONTEXT('part definition',#6442,'mechanical');
#6450=PRODUCT('Journal spacer (1)','Journal spacer (1)','Journal spacer (1)',
(#6443));
#6525=COLOUR_RGB('Sky Blue',0.24,0.69,0.87);
#6526=FILL_AREA_STYLE_COLOUR('',#6525);
#6527=FILL_AREA_STYLE('',(#6526));
#6528=SURFACE_STYLE_FILL_AREA(#6527);
#6529=SURFACE_SIDE_STYLE('',(#6528));
#6530=SURFACE_STYLE_USAGE(.BOTH.,#6529);
#6531=PRESENTATION_STYLE_ASSIGNMENT((#6530));
ENDSEC;
END-ISO-10303-21;
